ISO-10303-21;
HEADER;
/* Generated by software containing ST-Developer
 * from STEP Tools, Inc. (www.steptools.com) 
 */

FILE_DESCRIPTION(
/* description */ ('Hook toggle clamp'),
/* implementation_level */ '2;1');

FILE_NAME(
/* name */ 'M5x14 Cap Screw.step',
/* time_stamp */ '2026-10-27T21:56:56-07:00',
/* author */ (''),
/* organization */ (''),
/* preprocessor_version */ 'ST-DEVELOPER v20.2',
/* originating_system */ 'Autodesk Translation Framework v15.17.0.0',
/* authorisation */ '');

FILE_SCHEMA (('AUTOMOTIVE_DESIGN { 1 0 10303 214 3 1 1 }'));
ENDSEC;

DATA;
#10=MECHANICAL_DESIGN_GEOMETRIC_PRESENTATION_REPRESENTATION('',(#196),#5458);
#127=ORIENTED_CLOSED_SHELL('',*,#2977,.F.);
#128=BREP_WITH_VOIDS('Body1',#2978,(#127));
#148=CONICAL_SURFACE('',#3337,0.4,0.785398163397448);
#149=CONICAL_SURFACE('',#3341,0.41,0.785398163397448);
#150=CONICAL_SURFACE('',#3345,0.26,0.463647609000806);
#162=SHAPE_REPRESENTATION_RELATIONSHIP('SRR','None',#5544,#179);
#179=ADVANCED_BREP_SHAPE_REPRESENTATION('',(#128),#5446);
#196=STYLED_ITEM('',(#5724),#128);
#254=FACE_BOUND('',#699,.T.);
#341=PLANE('',#3325);
#342=PLANE('',#3326);
#343=PLANE('',#3327);
#344=PLANE('',#3328);
#345=PLANE('',#3329);
#346=PLANE('',#3330);
#347=PLANE('',#3331);
#348=PLANE('',#3332);
#349=PLANE('',#3333);
#350=PLANE('',#3335);
#351=PLANE('',#3343);
#480=FACE_OUTER_BOUND('',#685,.T.);
#481=FACE_OUTER_BOUND('',#686,.T.);
#482=FACE_OUTER_BOUND('',#687,.T.);
#483=FACE_OUTER_BOUND('',#688,.T.);
#484=FACE_OUTER_BOUND('',#689,.T.);
#485=FACE_OUTER_BOUND('',#690,.T.);
#486=FACE_OUTER_BOUND('',#691,.T.);
#487=FACE_OUTER_BOUND('',#692,.T.);
#488=FACE_OUTER_BOUND('',#693,.T.);
#489=FACE_OUTER_BOUND('',#694,.T.);
#490=FACE_OUTER_BOUND('',#695,.T.);
#491=FACE_OUTER_BOUND('',#696,.T.);
#492=FACE_OUTER_BOUND('',#697,.T.);
#493=FACE_OUTER_BOUND('',#698,.T.);
#494=FACE_OUTER_BOUND('',#700,.T.);
#495=FACE_OUTER_BOUND('',#701,.T.);
#685=EDGE_LOOP('',(#2401,#2402,#2403,#2404));
#686=EDGE_LOOP('',(#2405,#2406,#2407,#2408));
#687=EDGE_LOOP('',(#2409,#2410,#2411,#2412));
#688=EDGE_LOOP('',(#2413,#2414,#2415,#2416));
#689=EDGE_LOOP('',(#2417,#2418,#2419,#2420));
#690=EDGE_LOOP('',(#2421,#2422,#2423,#2424));
#691=EDGE_LOOP('',(#2425,#2426,#2427,#2428,#2429,#2430));
#692=EDGE_LOOP('',(#2431,#2432,#2433,#2434,#2435,#2436));
#693=EDGE_LOOP('',(#2437));
#694=EDGE_LOOP('',(#2438));
#695=EDGE_LOOP('',(#2439,#2440,#2441,#2442));
#696=EDGE_LOOP('',(#2443,#2444,#2445,#2446));
#697=EDGE_LOOP('',(#2447,#2448,#2449,#2450));
#698=EDGE_LOOP('',(#2451));
#699=EDGE_LOOP('',(#2452));
#700=EDGE_LOOP('',(#2453,#2454,#2455,#2456));
#701=EDGE_LOOP('',(#2457,#2458,#2459,#2460));
#938=LINE('',#4864,#1175);
#939=LINE('',#4866,#1176);
#940=LINE('',#4868,#1177);
#941=LINE('',#4869,#1178);
#942=LINE('',#4872,#1179);
#943=LINE('',#4874,#1180);
#944=LINE('',#4875,#1181);
#945=LINE('',#4878,#1182);
#946=LINE('',#4880,#1183);
#947=LINE('',#4881,#1184);
#948=LINE('',#4884,#1185);
#949=LINE('',#4886,#1186);
#950=LINE('',#4887,#1187);
#951=LINE('',#4890,#1188);
#952=LINE('',#4892,#1189);
#953=LINE('',#4893,#1190);
#954=LINE('',#4895,#1191);
#955=LINE('',#4896,#1192);
#956=LINE('',#4908,#1193);
#957=LINE('',#4912,#1194);
#958=LINE('',#4916,#1195);
#959=LINE('',#4923,#1196);
#960=LINE('',#4925,#1197);
#1175=VECTOR('',#3954,1.);
#1176=VECTOR('',#3955,1.);
#1177=VECTOR('',#3956,1.);
#1178=VECTOR('',#3957,1.);
#1179=VECTOR('',#3960,1.);
#1180=VECTOR('',#3961,1.);
#1181=VECTOR('',#3962,1.);
#1182=VECTOR('',#3965,1.);
#1183=VECTOR('',#3966,1.);
#1184=VECTOR('',#3967,1.);
#1185=VECTOR('',#3970,1.);
#1186=VECTOR('',#3971,1.);
#1187=VECTOR('',#3972,1.);
#1188=VECTOR('',#3975,1.);
#1189=VECTOR('',#3976,1.);
#1190=VECTOR('',#3977,1.);
#1191=VECTOR('',#3980,1.);
#1192=VECTOR('',#3981,1.);
#1193=VECTOR('',#3998,0.4);
#1194=VECTOR('',#4003,0.425);
#1195=VECTOR('',#4008,0.41);
#1196=VECTOR('',#4017,0.26);
#1197=VECTOR('',#4020,0.25);
#1320=CIRCLE('',#3334,0.24505);
#1321=CIRCLE('',#3336,0.375);
#1322=CIRCLE('',#3338,0.425);
#1323=CIRCLE('',#3340,0.425);
#1324=CIRCLE('',#3342,0.395);
#1325=CIRCLE('',#3344,0.27);
#1326=CIRCLE('',#3346,0.24505);
#1515=VERTEX_POINT('',#4862);
#1516=VERTEX_POINT('',#4863);
#1517=VERTEX_POINT('',#4865);
#1518=VERTEX_POINT('',#4867);
#1519=VERTEX_POINT('',#4871);
#1520=VERTEX_POINT('',#4873);
#1521=VERTEX_POINT('',#4877);
#1522=VERTEX_POINT('',#4879);
#1523=VERTEX_POINT('',#4883);
#1524=VERTEX_POINT('',#4885);
#1525=VERTEX_POINT('',#4889);
#1526=VERTEX_POINT('',#4891);
#1527=VERTEX_POINT('',#4900);
#1528=VERTEX_POINT('',#4903);
#1529=VERTEX_POINT('',#4906);
#1530=VERTEX_POINT('',#4910);
#1531=VERTEX_POINT('',#4914);
#1532=VERTEX_POINT('',#4918);
#1533=VERTEX_POINT('',#4921);
#1827=EDGE_CURVE('',#1515,#1516,#938,.T.);
#1828=EDGE_CURVE('',#1516,#1517,#939,.T.);
#1829=EDGE_CURVE('',#1517,#1518,#940,.T.);
#1830=EDGE_CURVE('',#1515,#1518,#941,.T.);
#1831=EDGE_CURVE('',#1516,#1519,#942,.T.);
#1832=EDGE_CURVE('',#1519,#1520,#943,.T.);
#1833=EDGE_CURVE('',#1520,#1517,#944,.T.);
#1834=EDGE_CURVE('',#1519,#1521,#945,.T.);
#1835=EDGE_CURVE('',#1521,#1522,#946,.T.);
#1836=EDGE_CURVE('',#1522,#1520,#947,.T.);
#1837=EDGE_CURVE('',#1521,#1523,#948,.T.);
#1838=EDGE_CURVE('',#1523,#1524,#949,.T.);
#1839=EDGE_CURVE('',#1524,#1522,#950,.T.);
#1840=EDGE_CURVE('',#1523,#1525,#951,.T.);
#1841=EDGE_CURVE('',#1525,#1526,#952,.T.);
#1842=EDGE_CURVE('',#1526,#1524,#953,.T.);
#1843=EDGE_CURVE('',#1525,#1515,#954,.T.);
#1844=EDGE_CURVE('',#1518,#1526,#955,.T.);
#1845=EDGE_CURVE('',#1527,#1527,#1320,.T.);
#1846=EDGE_CURVE('',#1528,#1528,#1321,.T.);
#1847=EDGE_CURVE('',#1529,#1529,#1322,.T.);
#1848=EDGE_CURVE('',#1529,#1528,#956,.T.);
#1849=EDGE_CURVE('',#1530,#1530,#1323,.T.);
#1850=EDGE_CURVE('',#1530,#1529,#957,.T.);
#1851=EDGE_CURVE('',#1531,#1531,#1324,.T.);
#1852=EDGE_CURVE('',#1531,#1530,#958,.T.);
#1853=EDGE_CURVE('',#1532,#1532,#1325,.T.);
#1854=EDGE_CURVE('',#1533,#1533,#1326,.F.);
#1855=EDGE_CURVE('',#1533,#1532,#959,.T.);
#1856=EDGE_CURVE('',#1527,#1533,#960,.T.);
#2401=ORIENTED_EDGE('',*,*,#1827,.T.);
#2402=ORIENTED_EDGE('',*,*,#1828,.T.);
#2403=ORIENTED_EDGE('',*,*,#1829,.T.);
#2404=ORIENTED_EDGE('',*,*,#1830,.F.);
#2405=ORIENTED_EDGE('',*,*,#1831,.T.);
#2406=ORIENTED_EDGE('',*,*,#1832,.T.);
#2407=ORIENTED_EDGE('',*,*,#1833,.T.);
#2408=ORIENTED_EDGE('',*,*,#1828,.F.);
#2409=ORIENTED_EDGE('',*,*,#1834,.T.);
#2410=ORIENTED_EDGE('',*,*,#1835,.T.);
#2411=ORIENTED_EDGE('',*,*,#1836,.T.);
#2412=ORIENTED_EDGE('',*,*,#1832,.F.);
#2413=ORIENTED_EDGE('',*,*,#1837,.T.);
#2414=ORIENTED_EDGE('',*,*,#1838,.T.);
#2415=ORIENTED_EDGE('',*,*,#1839,.T.);
#2416=ORIENTED_EDGE('',*,*,#1835,.F.);
#2417=ORIENTED_EDGE('',*,*,#1840,.T.);
#2418=ORIENTED_EDGE('',*,*,#1841,.T.);
#2419=ORIENTED_EDGE('',*,*,#1842,.T.);
#2420=ORIENTED_EDGE('',*,*,#1838,.F.);
#2421=ORIENTED_EDGE('',*,*,#1843,.T.);
#2422=ORIENTED_EDGE('',*,*,#1830,.T.);
#2423=ORIENTED_EDGE('',*,*,#1844,.T.);
#2424=ORIENTED_EDGE('',*,*,#1841,.F.);
#2425=ORIENTED_EDGE('',*,*,#1843,.F.);
#2426=ORIENTED_EDGE('',*,*,#1840,.F.);
#2427=ORIENTED_EDGE('',*,*,#1837,.F.);
#2428=ORIENTED_EDGE('',*,*,#1834,.F.);
#2429=ORIENTED_EDGE('',*,*,#1831,.F.);
#2430=ORIENTED_EDGE('',*,*,#1827,.F.);
#2431=ORIENTED_EDGE('',*,*,#1844,.F.);
#2432=ORIENTED_EDGE('',*,*,#1829,.F.);
#2433=ORIENTED_EDGE('',*,*,#1833,.F.);
#2434=ORIENTED_EDGE('',*,*,#1836,.F.);
#2435=ORIENTED_EDGE('',*,*,#1839,.F.);
#2436=ORIENTED_EDGE('',*,*,#1842,.F.);
#2437=ORIENTED_EDGE('',*,*,#1845,.F.);
#2438=ORIENTED_EDGE('',*,*,#1846,.F.);
#2439=ORIENTED_EDGE('',*,*,#1847,.F.);
#2440=ORIENTED_EDGE('',*,*,#1848,.T.);
#2441=ORIENTED_EDGE('',*,*,#1846,.T.);
#2442=ORIENTED_EDGE('',*,*,#1848,.F.);
#2443=ORIENTED_EDGE('',*,*,#1849,.F.);
#2444=ORIENTED_EDGE('',*,*,#1850,.T.);
#2445=ORIENTED_EDGE('',*,*,#1847,.T.);
#2446=ORIENTED_EDGE('',*,*,#1850,.F.);
#2447=ORIENTED_EDGE('',*,*,#1851,.F.);
#2448=ORIENTED_EDGE('',*,*,#1852,.T.);
#2449=ORIENTED_EDGE('',*,*,#1849,.T.);
#2450=ORIENTED_EDGE('',*,*,#1852,.F.);
#2451=ORIENTED_EDGE('',*,*,#1851,.T.);
#2452=ORIENTED_EDGE('',*,*,#1853,.F.);
#2453=ORIENTED_EDGE('',*,*,#1854,.F.);
#2454=ORIENTED_EDGE('',*,*,#1855,.T.);
#2455=ORIENTED_EDGE('',*,*,#1853,.T.);
#2456=ORIENTED_EDGE('',*,*,#1855,.F.);
#2457=ORIENTED_EDGE('',*,*,#1845,.T.);
#2458=ORIENTED_EDGE('',*,*,#1856,.T.);
#2459=ORIENTED_EDGE('',*,*,#1854,.T.);
#2460=ORIENTED_EDGE('',*,*,#1856,.F.);
#2772=CYLINDRICAL_SURFACE('',#3339,0.425);
#2773=CYLINDRICAL_SURFACE('',#3347,0.24505);
#2884=ADVANCED_FACE('',(#480),#341,.F.);
#2885=ADVANCED_FACE('',(#481),#342,.F.);
#2886=ADVANCED_FACE('',(#482),#343,.F.);
#2887=ADVANCED_FACE('',(#483),#344,.F.);
#2888=ADVANCED_FACE('',(#484),#345,.F.);
#2889=ADVANCED_FACE('',(#485),#346,.F.);
#2890=ADVANCED_FACE('',(#486),#347,.F.);
#2891=ADVANCED_FACE('',(#487),#348,.F.);
#2892=ADVANCED_FACE('',(#488),#349,.F.);
#2893=ADVANCED_FACE('',(#489),#350,.T.);
#2894=ADVANCED_FACE('',(#490),#148,.T.);
#2895=ADVANCED_FACE('',(#491),#2772,.T.);
#2896=ADVANCED_FACE('',(#492),#149,.T.);
#2897=ADVANCED_FACE('',(#493,#254),#351,.T.);
#2898=ADVANCED_FACE('',(#494),#150,.T.);
#2899=ADVANCED_FACE('',(#495),#2773,.T.);
#2977=CLOSED_SHELL('',(#2884,#2885,#2886,#2887,#2888,#2889,#2890,#2891));
#2978=CLOSED_SHELL('',(#2892,#2893,#2894,#2895,#2896,#2897,#2898,#2899));
#3324=AXIS2_PLACEMENT_3D('',#4860,#3950,#3951);
#3325=AXIS2_PLACEMENT_3D('',#4861,#3952,#3953);
#3326=AXIS2_PLACEMENT_3D('',#4870,#3958,#3959);
#3327=AXIS2_PLACEMENT_3D('',#4876,#3963,#3964);
#3328=AXIS2_PLACEMENT_3D('',#4882,#3968,#3969);
#3329=AXIS2_PLACEMENT_3D('',#4888,#3973,#3974);
#3330=AXIS2_PLACEMENT_3D('',#4894,#3978,#3979);
#3331=AXIS2_PLACEMENT_3D('',#4897,#3982,#3983);
#3332=AXIS2_PLACEMENT_3D('',#4898,#3984,#3985);
#3333=AXIS2_PLACEMENT_3D('',#4899,#3986,#3987);
#3334=AXIS2_PLACEMENT_3D('',#4901,#3988,#3989);
#3335=AXIS2_PLACEMENT_3D('',#4902,#3990,#3991);
#3336=AXIS2_PLACEMENT_3D('',#4904,#3992,#3993);
#3337=AXIS2_PLACEMENT_3D('',#4905,#3994,#3995);
#3338=AXIS2_PLACEMENT_3D('',#4907,#3996,#3997);
#3339=AXIS2_PLACEMENT_3D('',#4909,#3999,#4000);
#3340=AXIS2_PLACEMENT_3D('',#4911,#4001,#4002);
#3341=AXIS2_PLACEMENT_3D('',#4913,#4004,#4005);
#3342=AXIS2_PLACEMENT_3D('',#4915,#4006,#4007);
#3343=AXIS2_PLACEMENT_3D('',#4917,#4009,#4010);
#3344=AXIS2_PLACEMENT_3D('',#4919,#4011,#4012);
#3345=AXIS2_PLACEMENT_3D('',#4920,#4013,#4014);
#3346=AXIS2_PLACEMENT_3D('',#4922,#4015,#4016);
#3347=AXIS2_PLACEMENT_3D('',#4924,#4018,#4019);
#3950=DIRECTION('axis',(0.,0.,1.));
#3951=DIRECTION('refdir',(1.,0.,0.));
#3952=DIRECTION('center_axis',(0.866025403784439,0.,-0.5));
#3953=DIRECTION('ref_axis',(0.5,0.,0.866025403784439));
#3954=DIRECTION('',(-0.5,0.,-0.866025403784439));
#3955=DIRECTION('',(0.,-1.,0.));
#3956=DIRECTION('',(0.5,0.,0.866025403784439));
#3957=DIRECTION('',(0.,-1.,0.));
#3958=DIRECTION('center_axis',(1.20185167898973E-16,0.,-1.));
#3959=DIRECTION('ref_axis',(1.,0.,1.20185167898973E-16));
#3960=DIRECTION('',(-1.,0.,-1.20185167898973E-16));
#3961=DIRECTION('',(0.,-1.,0.));
#3962=DIRECTION('',(1.,0.,1.20185167898973E-16));
#3963=DIRECTION('center_axis',(-0.866025403784439,0.,-0.5));
#3964=DIRECTION('ref_axis',(0.5,0.,-0.866025403784439));
#3965=DIRECTION('',(-0.5,0.,0.866025403784439));
#3966=DIRECTION('',(0.,-1.,0.));
#3967=DIRECTION('',(0.5,0.,-0.866025403784439));
#3968=DIRECTION('center_axis',(-0.866025403784439,0.,0.5));
#3969=DIRECTION('ref_axis',(-0.5,0.,-0.866025403784439));
#3970=DIRECTION('',(0.5,0.,0.866025403784439));
#3971=DIRECTION('',(0.,-1.,0.));
#3972=DIRECTION('',(-0.5,0.,-0.866025403784439));
#3973=DIRECTION('center_axis',(-2.40370335797945E-16,0.,1.));
#3974=DIRECTION('ref_axis',(-1.,0.,-2.40370335797945E-16));
#3975=DIRECTION('',(1.,0.,2.40370335797945E-16));
#3976=DIRECTION('',(0.,-1.,0.));
#3977=DIRECTION('',(-1.,0.,-2.40370335797945E-16));
#3978=DIRECTION('center_axis',(0.866025403784439,0.,0.5));
#3979=DIRECTION('ref_axis',(-0.5,0.,0.866025403784439));
#3980=DIRECTION('',(0.5,0.,-0.866025403784439));
#3981=DIRECTION('',(-0.5,0.,0.866025403784439));
#3982=DIRECTION('center_axis',(0.,1.,0.));
#3983=DIRECTION('ref_axis',(1.,0.,0.));
#3984=DIRECTION('center_axis',(0.,-1.,0.));
#3985=DIRECTION('ref_axis',(0.,0.,-1.));
#3986=DIRECTION('center_axis',(0.,1.,0.));
#3987=DIRECTION('ref_axis',(1.,0.,0.));
#3988=DIRECTION('center_axis',(0.,1.,0.));
#3989=DIRECTION('ref_axis',(1.,0.,0.));
#3990=DIRECTION('center_axis',(0.,1.,0.));
#3991=DIRECTION('ref_axis',(0.,0.,1.));
#3992=DIRECTION('center_axis',(0.,-1.,0.));
#3993=DIRECTION('ref_axis',(1.,0.,0.));
#3994=DIRECTION('center_axis',(0.,-1.,0.));
#3995=DIRECTION('ref_axis',(1.,0.,0.));
#3996=DIRECTION('center_axis',(0.,-1.,0.));
#3997=DIRECTION('ref_axis',(1.,0.,0.));
#3998=DIRECTION('',(0.707106781186548,0.707106781186547,8.65956056235493E-17));
#3999=DIRECTION('center_axis',(0.,-1.,0.));
#4000=DIRECTION('ref_axis',(1.,0.,0.));
#4001=DIRECTION('center_axis',(0.,-1.,0.));
#4002=DIRECTION('ref_axis',(1.,0.,0.));
#4003=DIRECTION('',(0.,1.,0.));
#4004=DIRECTION('center_axis',(0.,1.,0.));
#4005=DIRECTION('ref_axis',(1.,0.,0.));
#4006=DIRECTION('center_axis',(0.,-1.,0.));
#4007=DIRECTION('ref_axis',(1.,0.,0.));
#4008=DIRECTION('',(-0.707106781186547,0.707106781186548,-8.65956056235493E-17));
#4009=DIRECTION('center_axis',(0.,-1.,0.));
#4010=DIRECTION('ref_axis',(0.,0.,-1.));
#4011=DIRECTION('center_axis',(0.,-1.,0.));
#4012=DIRECTION('ref_axis',(1.,0.,0.));
#4013=DIRECTION('center_axis',(0.,1.,0.));
#4014=DIRECTION('ref_axis',(1.,0.,0.));
#4015=DIRECTION('center_axis',(0.,1.,0.));
#4016=DIRECTION('ref_axis',(1.,0.,0.));
#4017=DIRECTION('',(-0.447213595499958,0.894427190999916,-5.47678698264203E-17));
#4018=DIRECTION('center_axis',(0.,-1.,0.));
#4019=DIRECTION('ref_axis',(1.,0.,0.));
#4020=DIRECTION('',(0.,1.,0.));
#4860=CARTESIAN_POINT('',(0.,0.,0.));
#4861=CARTESIAN_POINT('Origin',(0.115470053837925,-0.5,-0.2));
#4862=CARTESIAN_POINT('',(0.23094010767585,-0.5,0.));
#4863=CARTESIAN_POINT('',(0.115470053837925,-0.5,-0.2));
#4864=CARTESIAN_POINT('',(0.23094010767585,-0.5,0.));
#4865=CARTESIAN_POINT('',(0.115470053837925,-0.8,-0.2));
#4866=CARTESIAN_POINT('',(0.115470053837925,-0.5,-0.2));
#4867=CARTESIAN_POINT('',(0.23094010767585,-0.8,0.));
#4868=CARTESIAN_POINT('',(0.23094010767585,-0.8,0.));
#4869=CARTESIAN_POINT('',(0.23094010767585,-0.5,0.));
#4870=CARTESIAN_POINT('Origin',(-0.115470053837925,-0.5,-0.2));
#4871=CARTESIAN_POINT('',(-0.115470053837925,-0.5,-0.2));
#4872=CARTESIAN_POINT('',(0.115470053837925,-0.5,-0.2));
#4873=CARTESIAN_POINT('',(-0.115470053837925,-0.8,-0.2));
#4874=CARTESIAN_POINT('',(-0.115470053837925,-0.5,-0.2));
#4875=CARTESIAN_POINT('',(0.115470053837925,-0.8,-0.2));
#4876=CARTESIAN_POINT('Origin',(-0.23094010767585,-0.5,-2.77555756156289E-17));
#4877=CARTESIAN_POINT('',(-0.23094010767585,-0.5,-2.82820063659975E-17));
#4878=CARTESIAN_POINT('',(-0.115470053837925,-0.5,-0.2));
#4879=CARTESIAN_POINT('',(-0.23094010767585,-0.8,-2.77555756156289E-17));
#4880=CARTESIAN_POINT('',(-0.23094010767585,-0.5,-2.82820063659975E-17));
#4881=CARTESIAN_POINT('',(-0.115470053837925,-0.8,-0.2));
#4882=CARTESIAN_POINT('Origin',(-0.115470053837925,-0.5,0.2));
#4883=CARTESIAN_POINT('',(-0.115470053837925,-0.5,0.2));
#4884=CARTESIAN_POINT('',(-0.23094010767585,-0.5,-2.82820063659975E-17));
#4885=CARTESIAN_POINT('',(-0.115470053837925,-0.8,0.2));
#4886=CARTESIAN_POINT('',(-0.115470053837925,-0.5,0.2));
#4887=CARTESIAN_POINT('',(-0.23094010767585,-0.8,-2.82820063659975E-17));
#4888=CARTESIAN_POINT('Origin',(0.115470053837925,-0.5,0.2));
#4889=CARTESIAN_POINT('',(0.115470053837925,-0.5,0.2));
#4890=CARTESIAN_POINT('',(-0.115470053837925,-0.5,0.2));
#4891=CARTESIAN_POINT('',(0.115470053837925,-0.8,0.2));
#4892=CARTESIAN_POINT('',(0.115470053837925,-0.5,0.2));
#4893=CARTESIAN_POINT('',(-0.115470053837925,-0.8,0.2));
#4894=CARTESIAN_POINT('Origin',(0.23094010767585,-0.5,0.));
#4895=CARTESIAN_POINT('',(0.115470053837925,-0.5,0.2));
#4896=CARTESIAN_POINT('',(0.115470053837925,-0.8,0.2));
#4897=CARTESIAN_POINT('Origin',(0.,-0.5,0.));
#4898=CARTESIAN_POINT('Origin',(0.,-0.8,0.));
#4899=CARTESIAN_POINT('Origin',(0.,-1.4,0.));
#4900=CARTESIAN_POINT('',(-0.24505,-1.4,3.00099698131059E-17));
#4901=CARTESIAN_POINT('Origin',(0.,-1.4,0.));
#4902=CARTESIAN_POINT('Origin',(0.375,0.5,0.));
#4903=CARTESIAN_POINT('',(-0.375,0.5,-4.59242549680257E-17));
#4904=CARTESIAN_POINT('Origin',(0.,0.5,0.));
#4905=CARTESIAN_POINT('Origin',(0.,0.475,0.));
#4906=CARTESIAN_POINT('',(-0.425,0.45,-5.20474889637625E-17));
#4907=CARTESIAN_POINT('Origin',(0.,0.45,0.));
#4908=CARTESIAN_POINT('',(-0.4,0.475,-4.89858719658941E-17));
#4909=CARTESIAN_POINT('Origin',(0.,0.24,0.));
#4910=CARTESIAN_POINT('',(-0.425,0.0299999999999998,-5.20474889637625E-17));
#4911=CARTESIAN_POINT('Origin',(0.,0.0299999999999998,0.));
#4912=CARTESIAN_POINT('',(-0.425,0.24,-5.20474889637625E-17));
#4913=CARTESIAN_POINT('Origin',(0.,0.0150000000000001,0.));
#4914=CARTESIAN_POINT('',(-0.395,4.85722573273506E-17,-4.83735485663204E-17));
#4915=CARTESIAN_POINT('Origin',(0.,0.,0.));
#4916=CARTESIAN_POINT('',(-0.41,0.0150000000000001,-5.02105187650415E-17));
#4917=CARTESIAN_POINT('Origin',(0.27,0.,0.));
#4918=CARTESIAN_POINT('',(-0.27,0.,-3.30654635769785E-17));
#4919=CARTESIAN_POINT('Origin',(0.,0.,0.));
#4920=CARTESIAN_POINT('Origin',(0.,-0.02,0.));
#4921=CARTESIAN_POINT('',(-0.24505,-0.0498999999999999,3.00099698131059E-17));
#4922=CARTESIAN_POINT('Origin',(0.,-0.0498999999999999,0.));
#4923=CARTESIAN_POINT('',(-0.26,-0.02,-3.18408167778312E-17));
#4924=CARTESIAN_POINT('Origin',(0.,-0.995,0.));
#4925=CARTESIAN_POINT('',(-0.24505,-0.995,-3.00099698131059E-17));
#5423=UNCERTAINTY_MEASURE_WITH_UNIT(LENGTH_MEASURE(0.001),#5459,
'DISTANCE_ACCURACY_VALUE',
'Maximum model space distance between geometric entities at asserted c
onnectivities');
#5435=UNCERTAINTY_MEASURE_WITH_UNIT(LENGTH_MEASURE(0.001),#5459,
'DISTANCE_ACCURACY_VALUE',
'Maximum model space distance between geometric entities at asserted c
onnectivities');
#5446=(
GEOMETRIC_REPRESENTATION_CONTEXT(3)
GLOBAL_UNCERTAINTY_ASSIGNED_CONTEXT((#5423))
GLOBAL_UNIT_ASSIGNED_CONTEXT((#5459,#5461,#5462))
REPRESENTATION_CONTEXT('','3D')
);
#5458=(
GEOMETRIC_REPRESENTATION_CONTEXT(3)
GLOBAL_UNCERTAINTY_ASSIGNED_CONTEXT((#5435))
GLOBAL_UNIT_ASSIGNED_CONTEXT((#5459,#5461,#5462))
REPRESENTATION_CONTEXT('','3D')
);
#5459=(
LENGTH_UNIT()
NAMED_UNIT(*)
SI_UNIT(.CENTI.,.METRE.)
);
#5461=(
NAMED_UNIT(*)
PLANE_ANGLE_UNIT()
SI_UNIT($,.RADIAN.)
);
#5462=(
NAMED_UNIT(*)
SI_UNIT($,.STERADIAN.)
SOLID_ANGLE_UNIT()
);
#5473=SHAPE_DEFINITION_REPRESENTATION(#5495,#5544);
#5495=PRODUCT_DEFINITION_SHAPE('',$,#5567);
#5544=SHAPE_REPRESENTATION('',(#3324),#5446);
#5556=PRODUCT_DEFINITION_CONTEXT('part definition',#5624,'design');
#5567=PRODUCT_DEFINITION('M5x14 Cap Screw','M5x14 Cap Screw',#5589,#5556);
#5589=PRODUCT_DEFINITION_FORMATION('',$,#5636);
#5624=APPLICATION_CONTEXT(
'Core Data for Automotive Mechanical Design Process');
#5625=PRODUCT_CONTEXT('part definition',#5624,'mechanical');
#5636=PRODUCT('M5x14 Cap Screw','M5x14 Cap Screw','M5x14 Cap Screw',(#5625));
#5718=COLOUR_RGB('Black',0.12,0.14,0.17);
#5719=FILL_AREA_STYLE_COLOUR('',#5718);
#5720=FILL_AREA_STYLE('',(#5719));
#5721=SURFACE_STYLE_FILL_AREA(#5720);
#5722=SURFACE_SIDE_STYLE('',(#5721));
#5723=SURFACE_STYLE_USAGE(.BOTH.,#5722);
#5724=PRESENTATION_STYLE_ASSIGNMENT((#5723));
ENDSEC;
END-ISO-10303-21;
